ISO-10303-21;
HEADER;
/* Generated by software containing ST-Developer
 * from STEP Tools, Inc. (www.steptools.com) 
 */

FILE_DESCRIPTION(
/* description */ ('Bearing-mounted hook block'),
/* implementation_level */ '2;1');

FILE_NAME(
/* name */ 'M4x10 Cap Screw.step',
/* time_stamp */ '2026-10-28T22:30:11-07:00',
/* author */ (''),
/* organization */ (''),
/* preprocessor_version */ 'ST-DEVELOPER v20.2',
/* originating_system */ 'Autodesk Translation Framework v15.17.0.0',
/* authorisation */ '');

FILE_SCHEMA (('AUTOMOTIVE_DESIGN { 1 0 10303 214 3 1 1 }'));
ENDSEC;

DATA;
#10=MECHANICAL_DESIGN_GEOMETRIC_PRESENTATION_REPRESENTATION('',(#351),#7609);
#266=CONICAL_SURFACE('',#4675,0.325,0.785398163397448);
#267=CONICAL_SURFACE('',#4679,0.335,0.785398163397448);
#268=CONICAL_SURFACE('',#4683,0.21,0.463647609000806);
#271=ORIENTED_CLOSED_SHELL('',*,#3949,.F.);
#274=BREP_WITH_VOIDS('Body1',#3950,(#271));
#295=SHAPE_REPRESENTATION_RELATIONSHIP('SRR','None',#7744,#319);
#319=ADVANCED_BREP_SHAPE_REPRESENTATION('',(#274),#7604);
#351=STYLED_ITEM('',(#7938),#274);
#548=LINE('',#7334,#778);
#549=LINE('',#7336,#779);
#550=LINE('',#7338,#780);
#551=LINE('',#7339,#781);
#552=LINE('',#7342,#782);
#553=LINE('',#7344,#783);
#554=LINE('',#7345,#784);
#555=LINE('',#7348,#785);
#556=LINE('',#7350,#786);
#557=LINE('',#7351,#787);
#558=LINE('',#7354,#788);
#559=LINE('',#7356,#789);
#560=LINE('',#7357,#790);
#561=LINE('',#7360,#791);
#562=LINE('',#7362,#792);
#563=LINE('',#7363,#793);
#564=LINE('',#7365,#794);
#565=LINE('',#7366,#795);
#566=LINE('',#7378,#796);
#567=LINE('',#7382,#797);
#568=LINE('',#7386,#798);
#569=LINE('',#7393,#799);
#570=LINE('',#7395,#800);
#778=VECTOR('',#5811,1.);
#779=VECTOR('',#5812,1.);
#780=VECTOR('',#5813,1.);
#781=VECTOR('',#5814,1.);
#782=VECTOR('',#5817,1.);
#783=VECTOR('',#5818,1.);
#784=VECTOR('',#5819,1.);
#785=VECTOR('',#5822,1.);
#786=VECTOR('',#5823,1.);
#787=VECTOR('',#5824,1.);
#788=VECTOR('',#5827,1.);
#789=VECTOR('',#5828,1.);
#790=VECTOR('',#5829,1.);
#791=VECTOR('',#5832,1.);
#792=VECTOR('',#5833,1.);
#793=VECTOR('',#5834,1.);
#794=VECTOR('',#5837,1.);
#795=VECTOR('',#5838,1.);
#796=VECTOR('',#5855,0.325);
#797=VECTOR('',#5860,0.35);
#798=VECTOR('',#5865,0.335);
#799=VECTOR('',#5874,0.21);
#800=VECTOR('',#5877,0.2);
#911=CYLINDRICAL_SURFACE('',#4677,0.35);
#912=CYLINDRICAL_SURFACE('',#4685,0.1954);
#994=FACE_BOUND('',#1515,.T.);
#1192=FACE_OUTER_BOUND('',#1501,.T.);
#1193=FACE_OUTER_BOUND('',#1502,.T.);
#1194=FACE_OUTER_BOUND('',#1503,.T.);
#1195=FACE_OUTER_BOUND('',#1504,.T.);
#1196=FACE_OUTER_BOUND('',#1505,.T.);
#1197=FACE_OUTER_BOUND('',#1506,.T.);
#1198=FACE_OUTER_BOUND('',#1507,.T.);
#1199=FACE_OUTER_BOUND('',#1508,.T.);
#1200=FACE_OUTER_BOUND('',#1509,.T.);
#1201=FACE_OUTER_BOUND('',#1510,.T.);
#1202=FACE_OUTER_BOUND('',#1511,.T.);
#1203=FACE_OUTER_BOUND('',#1512,.T.);
#1204=FACE_OUTER_BOUND('',#1513,.T.);
#1205=FACE_OUTER_BOUND('',#1514,.T.);
#1206=FACE_OUTER_BOUND('',#1516,.T.);
#1207=FACE_OUTER_BOUND('',#1517,.T.);
#1501=EDGE_LOOP('',(#3378,#3379,#3380,#3381));
#1502=EDGE_LOOP('',(#3382,#3383,#3384,#3385));
#1503=EDGE_LOOP('',(#3386,#3387,#3388,#3389));
#1504=EDGE_LOOP('',(#3390,#3391,#3392,#3393));
#1505=EDGE_LOOP('',(#3394,#3395,#3396,#3397));
#1506=EDGE_LOOP('',(#3398,#3399,#3400,#3401));
#1507=EDGE_LOOP('',(#3402,#3403,#3404,#3405,#3406,#3407));
#1508=EDGE_LOOP('',(#3408,#3409,#3410,#3411,#3412,#3413));
#1509=EDGE_LOOP('',(#3414));
#1510=EDGE_LOOP('',(#3415));
#1511=EDGE_LOOP('',(#3416,#3417,#3418,#3419));
#1512=EDGE_LOOP('',(#3420,#3421,#3422,#3423));
#1513=EDGE_LOOP('',(#3424,#3425,#3426,#3427));
#1514=EDGE_LOOP('',(#3428));
#1515=EDGE_LOOP('',(#3429));
#1516=EDGE_LOOP('',(#3430,#3431,#3432,#3433));
#1517=EDGE_LOOP('',(#3434,#3435,#3436,#3437));
#1753=CIRCLE('',#4672,0.1954);
#1754=CIRCLE('',#4674,0.3);
#1755=CIRCLE('',#4676,0.35);
#1756=CIRCLE('',#4678,0.35);
#1757=CIRCLE('',#4680,0.32);
#1758=CIRCLE('',#4682,0.22);
#1759=CIRCLE('',#4684,0.1954);
#2046=VERTEX_POINT('',#7332);
#2047=VERTEX_POINT('',#7333);
#2048=VERTEX_POINT('',#7335);
#2049=VERTEX_POINT('',#7337);
#2050=VERTEX_POINT('',#7341);
#2051=VERTEX_POINT('',#7343);
#2052=VERTEX_POINT('',#7347);
#2053=VERTEX_POINT('',#7349);
#2054=VERTEX_POINT('',#7353);
#2055=VERTEX_POINT('',#7355);
#2056=VERTEX_POINT('',#7359);
#2057=VERTEX_POINT('',#7361);
#2058=VERTEX_POINT('',#7370);
#2059=VERTEX_POINT('',#7373);
#2060=VERTEX_POINT('',#7376);
#2061=VERTEX_POINT('',#7380);
#2062=VERTEX_POINT('',#7384);
#2063=VERTEX_POINT('',#7388);
#2064=VERTEX_POINT('',#7391);
#2499=EDGE_CURVE('',#2046,#2047,#548,.T.);
#2500=EDGE_CURVE('',#2047,#2048,#549,.T.);
#2501=EDGE_CURVE('',#2048,#2049,#550,.T.);
#2502=EDGE_CURVE('',#2046,#2049,#551,.T.);
#2503=EDGE_CURVE('',#2047,#2050,#552,.T.);
#2504=EDGE_CURVE('',#2050,#2051,#553,.T.);
#2505=EDGE_CURVE('',#2051,#2048,#554,.T.);
#2506=EDGE_CURVE('',#2050,#2052,#555,.T.);
#2507=EDGE_CURVE('',#2052,#2053,#556,.T.);
#2508=EDGE_CURVE('',#2053,#2051,#557,.T.);
#2509=EDGE_CURVE('',#2052,#2054,#558,.T.);
#2510=EDGE_CURVE('',#2054,#2055,#559,.T.);
#2511=EDGE_CURVE('',#2055,#2053,#560,.T.);
#2512=EDGE_CURVE('',#2054,#2056,#561,.T.);
#2513=EDGE_CURVE('',#2056,#2057,#562,.T.);
#2514=EDGE_CURVE('',#2057,#2055,#563,.T.);
#2515=EDGE_CURVE('',#2056,#2046,#564,.T.);
#2516=EDGE_CURVE('',#2049,#2057,#565,.T.);
#2517=EDGE_CURVE('',#2058,#2058,#1753,.T.);
#2518=EDGE_CURVE('',#2059,#2059,#1754,.T.);
#2519=EDGE_CURVE('',#2060,#2060,#1755,.T.);
#2520=EDGE_CURVE('',#2060,#2059,#566,.T.);
#2521=EDGE_CURVE('',#2061,#2061,#1756,.T.);
#2522=EDGE_CURVE('',#2061,#2060,#567,.T.);
#2523=EDGE_CURVE('',#2062,#2062,#1757,.T.);
#2524=EDGE_CURVE('',#2062,#2061,#568,.T.);
#2525=EDGE_CURVE('',#2063,#2063,#1758,.T.);
#2526=EDGE_CURVE('',#2064,#2064,#1759,.F.);
#2527=EDGE_CURVE('',#2064,#2063,#569,.T.);
#2528=EDGE_CURVE('',#2058,#2064,#570,.T.);
#3378=ORIENTED_EDGE('',*,*,#2499,.T.);
#3379=ORIENTED_EDGE('',*,*,#2500,.T.);
#3380=ORIENTED_EDGE('',*,*,#2501,.T.);
#3381=ORIENTED_EDGE('',*,*,#2502,.F.);
#3382=ORIENTED_EDGE('',*,*,#2503,.T.);
#3383=ORIENTED_EDGE('',*,*,#2504,.T.);
#3384=ORIENTED_EDGE('',*,*,#2505,.T.);
#3385=ORIENTED_EDGE('',*,*,#2500,.F.);
#3386=ORIENTED_EDGE('',*,*,#2506,.T.);
#3387=ORIENTED_EDGE('',*,*,#2507,.T.);
#3388=ORIENTED_EDGE('',*,*,#2508,.T.);
#3389=ORIENTED_EDGE('',*,*,#2504,.F.);
#3390=ORIENTED_EDGE('',*,*,#2509,.T.);
#3391=ORIENTED_EDGE('',*,*,#2510,.T.);
#3392=ORIENTED_EDGE('',*,*,#2511,.T.);
#3393=ORIENTED_EDGE('',*,*,#2507,.F.);
#3394=ORIENTED_EDGE('',*,*,#2512,.T.);
#3395=ORIENTED_EDGE('',*,*,#2513,.T.);
#3396=ORIENTED_EDGE('',*,*,#2514,.T.);
#3397=ORIENTED_EDGE('',*,*,#2510,.F.);
#3398=ORIENTED_EDGE('',*,*,#2515,.T.);
#3399=ORIENTED_EDGE('',*,*,#2502,.T.);
#3400=ORIENTED_EDGE('',*,*,#2516,.T.);
#3401=ORIENTED_EDGE('',*,*,#2513,.F.);
#3402=ORIENTED_EDGE('',*,*,#2515,.F.);
#3403=ORIENTED_EDGE('',*,*,#2512,.F.);
#3404=ORIENTED_EDGE('',*,*,#2509,.F.);
#3405=ORIENTED_EDGE('',*,*,#2506,.F.);
#3406=ORIENTED_EDGE('',*,*,#2503,.F.);
#3407=ORIENTED_EDGE('',*,*,#2499,.F.);
#3408=ORIENTED_EDGE('',*,*,#2516,.F.);
#3409=ORIENTED_EDGE('',*,*,#2501,.F.);
#3410=ORIENTED_EDGE('',*,*,#2505,.F.);
#3411=ORIENTED_EDGE('',*,*,#2508,.F.);
#3412=ORIENTED_EDGE('',*,*,#2511,.F.);
#3413=ORIENTED_EDGE('',*,*,#2514,.F.);
#3414=ORIENTED_EDGE('',*,*,#2517,.F.);
#3415=ORIENTED_EDGE('',*,*,#2518,.F.);
#3416=ORIENTED_EDGE('',*,*,#2519,.F.);
#3417=ORIENTED_EDGE('',*,*,#2520,.T.);
#3418=ORIENTED_EDGE('',*,*,#2518,.T.);
#3419=ORIENTED_EDGE('',*,*,#2520,.F.);
#3420=ORIENTED_EDGE('',*,*,#2521,.F.);
#3421=ORIENTED_EDGE('',*,*,#2522,.T.);
#3422=ORIENTED_EDGE('',*,*,#2519,.T.);
#3423=ORIENTED_EDGE('',*,*,#2522,.F.);
#3424=ORIENTED_EDGE('',*,*,#2523,.F.);
#3425=ORIENTED_EDGE('',*,*,#2524,.T.);
#3426=ORIENTED_EDGE('',*,*,#2521,.T.);
#3427=ORIENTED_EDGE('',*,*,#2524,.F.);
#3428=ORIENTED_EDGE('',*,*,#2523,.T.);
#3429=ORIENTED_EDGE('',*,*,#2525,.F.);
#3430=ORIENTED_EDGE('',*,*,#2526,.F.);
#3431=ORIENTED_EDGE('',*,*,#2527,.T.);
#3432=ORIENTED_EDGE('',*,*,#2525,.T.);
#3433=ORIENTED_EDGE('',*,*,#2527,.F.);
#3434=ORIENTED_EDGE('',*,*,#2517,.T.);
#3435=ORIENTED_EDGE('',*,*,#2528,.T.);
#3436=ORIENTED_EDGE('',*,*,#2526,.T.);
#3437=ORIENTED_EDGE('',*,*,#2528,.F.);
#3651=PLANE('',#4663);
#3652=PLANE('',#4664);
#3653=PLANE('',#4665);
#3654=PLANE('',#4666);
#3655=PLANE('',#4667);
#3656=PLANE('',#4668);
#3657=PLANE('',#4669);
#3658=PLANE('',#4670);
#3659=PLANE('',#4671);
#3660=PLANE('',#4673);
#3661=PLANE('',#4681);
#3874=ADVANCED_FACE('',(#1192),#3651,.F.);
#3875=ADVANCED_FACE('',(#1193),#3652,.F.);
#3876=ADVANCED_FACE('',(#1194),#3653,.F.);
#3877=ADVANCED_FACE('',(#1195),#3654,.F.);
#3878=ADVANCED_FACE('',(#1196),#3655,.F.);
#3879=ADVANCED_FACE('',(#1197),#3656,.F.);
#3880=ADVANCED_FACE('',(#1198),#3657,.F.);
#3881=ADVANCED_FACE('',(#1199),#3658,.F.);
#3882=ADVANCED_FACE('',(#1200),#3659,.F.);
#3883=ADVANCED_FACE('',(#1201),#3660,.T.);
#3884=ADVANCED_FACE('',(#1202),#266,.T.);
#3885=ADVANCED_FACE('',(#1203),#911,.T.);
#3886=ADVANCED_FACE('',(#1204),#267,.T.);
#3887=ADVANCED_FACE('',(#1205,#994),#3661,.T.);
#3888=ADVANCED_FACE('',(#1206),#268,.T.);
#3889=ADVANCED_FACE('',(#1207),#912,.T.);
#3949=CLOSED_SHELL('',(#3874,#3875,#3876,#3877,#3878,#3879,#3880,#3881));
#3950=CLOSED_SHELL('',(#3882,#3883,#3884,#3885,#3886,#3887,#3888,#3889));
#4662=AXIS2_PLACEMENT_3D('',#7330,#5807,#5808);
#4663=AXIS2_PLACEMENT_3D('',#7331,#5809,#5810);
#4664=AXIS2_PLACEMENT_3D('',#7340,#5815,#5816);
#4665=AXIS2_PLACEMENT_3D('',#7346,#5820,#5821);
#4666=AXIS2_PLACEMENT_3D('',#7352,#5825,#5826);
#4667=AXIS2_PLACEMENT_3D('',#7358,#5830,#5831);
#4668=AXIS2_PLACEMENT_3D('',#7364,#5835,#5836);
#4669=AXIS2_PLACEMENT_3D('',#7367,#5839,#5840);
#4670=AXIS2_PLACEMENT_3D('',#7368,#5841,#5842);
#4671=AXIS2_PLACEMENT_3D('',#7369,#5843,#5844);
#4672=AXIS2_PLACEMENT_3D('',#7371,#5845,#5846);
#4673=AXIS2_PLACEMENT_3D('',#7372,#5847,#5848);
#4674=AXIS2_PLACEMENT_3D('',#7374,#5849,#5850);
#4675=AXIS2_PLACEMENT_3D('',#7375,#5851,#5852);
#4676=AXIS2_PLACEMENT_3D('',#7377,#5853,#5854);
#4677=AXIS2_PLACEMENT_3D('',#7379,#5856,#5857);
#4678=AXIS2_PLACEMENT_3D('',#7381,#5858,#5859);
#4679=AXIS2_PLACEMENT_3D('',#7383,#5861,#5862);
#4680=AXIS2_PLACEMENT_3D('',#7385,#5863,#5864);
#4681=AXIS2_PLACEMENT_3D('',#7387,#5866,#5867);
#4682=AXIS2_PLACEMENT_3D('',#7389,#5868,#5869);
#4683=AXIS2_PLACEMENT_3D('',#7390,#5870,#5871);
#4684=AXIS2_PLACEMENT_3D('',#7392,#5872,#5873);
#4685=AXIS2_PLACEMENT_3D('',#7394,#5875,#5876);
#5807=DIRECTION('axis',(0.,0.,1.));
#5808=DIRECTION('refdir',(1.,0.,0.));
#5809=DIRECTION('center_axis',(0.866025403784439,0.,-0.5));
#5810=DIRECTION('ref_axis',(0.5,0.,0.866025403784439));
#5811=DIRECTION('',(-0.5,0.,-0.866025403784439));
#5812=DIRECTION('',(0.,-1.,0.));
#5813=DIRECTION('',(0.5,0.,0.866025403784439));
#5814=DIRECTION('',(0.,-1.,0.));
#5815=DIRECTION('center_axis',(1.60246890531964E-16,0.,-1.));
#5816=DIRECTION('ref_axis',(1.,0.,1.60246890531964E-16));
#5817=DIRECTION('',(-1.,0.,-1.60246890531964E-16));
#5818=DIRECTION('',(0.,-1.,0.));
#5819=DIRECTION('',(1.,0.,1.60246890531964E-16));
#5820=DIRECTION('center_axis',(-0.866025403784439,0.,-0.5));
#5821=DIRECTION('ref_axis',(0.5,0.,-0.866025403784439));
#5822=DIRECTION('',(-0.5,0.,0.866025403784439));
#5823=DIRECTION('',(0.,-1.,0.));
#5824=DIRECTION('',(0.5,0.,-0.866025403784439));
#5825=DIRECTION('center_axis',(-0.866025403784439,0.,0.5));
#5826=DIRECTION('ref_axis',(-0.5,0.,-0.866025403784439));
#5827=DIRECTION('',(0.5,0.,0.866025403784439));
#5828=DIRECTION('',(0.,-1.,0.));
#5829=DIRECTION('',(-0.5,0.,-0.866025403784439));
#5830=DIRECTION('center_axis',(-1.60246890531964E-16,0.,1.));
#5831=DIRECTION('ref_axis',(-1.,0.,-1.60246890531964E-16));
#5832=DIRECTION('',(1.,0.,1.60246890531964E-16));
#5833=DIRECTION('',(0.,-1.,0.));
#5834=DIRECTION('',(-1.,0.,-1.60246890531964E-16));
#5835=DIRECTION('center_axis',(0.866025403784439,0.,0.5));
#5836=DIRECTION('ref_axis',(-0.5,0.,0.866025403784439));
#5837=DIRECTION('',(0.5,0.,-0.866025403784439));
#5838=DIRECTION('',(-0.5,0.,0.866025403784439));
#5839=DIRECTION('center_axis',(0.,1.,0.));
#5840=DIRECTION('ref_axis',(1.,0.,0.));
#5841=DIRECTION('center_axis',(0.,-1.,0.));
#5842=DIRECTION('ref_axis',(0.,0.,-1.));
#5843=DIRECTION('center_axis',(0.,1.,0.));
#5844=DIRECTION('ref_axis',(1.,0.,0.));
#5845=DIRECTION('center_axis',(0.,1.,0.));
#5846=DIRECTION('ref_axis',(1.,0.,0.));
#5847=DIRECTION('center_axis',(0.,1.,0.));
#5848=DIRECTION('ref_axis',(0.,0.,1.));
#5849=DIRECTION('center_axis',(0.,-1.,0.));
#5850=DIRECTION('ref_axis',(1.,0.,0.));
#5851=DIRECTION('center_axis',(0.,-1.,0.));
#5852=DIRECTION('ref_axis',(1.,0.,0.));
#5853=DIRECTION('center_axis',(0.,-1.,0.));
#5854=DIRECTION('ref_axis',(1.,0.,0.));
#5855=DIRECTION('',(0.707106781186547,0.707106781186548,8.65956056235493E-17));
#5856=DIRECTION('center_axis',(0.,-1.,0.));
#5857=DIRECTION('ref_axis',(1.,0.,0.));
#5858=DIRECTION('center_axis',(0.,-1.,0.));
#5859=DIRECTION('ref_axis',(1.,0.,0.));
#5860=DIRECTION('',(0.,1.,0.));
#5861=DIRECTION('center_axis',(0.,1.,0.));
#5862=DIRECTION('ref_axis',(1.,0.,0.));
#5863=DIRECTION('center_axis',(0.,-1.,0.));
#5864=DIRECTION('ref_axis',(1.,0.,0.));
#5865=DIRECTION('',(-0.707106781186547,0.707106781186548,-8.65956056235493E-17));
#5866=DIRECTION('center_axis',(0.,-1.,0.));
#5867=DIRECTION('ref_axis',(0.,0.,-1.));
#5868=DIRECTION('center_axis',(0.,-1.,0.));
#5869=DIRECTION('ref_axis',(1.,0.,0.));
#5870=DIRECTION('center_axis',(0.,1.,0.));
#5871=DIRECTION('ref_axis',(1.,0.,0.));
#5872=DIRECTION('center_axis',(0.,1.,0.));
#5873=DIRECTION('ref_axis',(1.,0.,0.));
#5874=DIRECTION('',(-0.447213595499958,0.894427190999916,-5.47678698264203E-17));
#5875=DIRECTION('center_axis',(0.,-1.,0.));
#5876=DIRECTION('ref_axis',(1.,0.,0.));
#5877=DIRECTION('',(0.,1.,0.));
#7330=CARTESIAN_POINT('',(0.,0.,0.));
#7331=CARTESIAN_POINT('Origin',(0.0866025403784439,-0.4,-0.15));
#7332=CARTESIAN_POINT('',(0.173205080756888,-0.4,0.));
#7333=CARTESIAN_POINT('',(0.0866025403784439,-0.4,-0.15));
#7334=CARTESIAN_POINT('',(0.173205080756888,-0.4,0.));
#7335=CARTESIAN_POINT('',(0.0866025403784439,-0.64,-0.15));
#7336=CARTESIAN_POINT('',(0.0866025403784439,-0.4,-0.15));
#7337=CARTESIAN_POINT('',(0.173205080756888,-0.64,0.));
#7338=CARTESIAN_POINT('',(0.173205080756888,-0.64,0.));
#7339=CARTESIAN_POINT('',(0.173205080756888,-0.4,0.));
#7340=CARTESIAN_POINT('Origin',(-0.0866025403784438,-0.4,-0.15));
#7341=CARTESIAN_POINT('',(-0.0866025403784438,-0.4,-0.15));
#7342=CARTESIAN_POINT('',(0.0866025403784439,-0.4,-0.15));
#7343=CARTESIAN_POINT('',(-0.0866025403784438,-0.64,-0.15));
#7344=CARTESIAN_POINT('',(-0.0866025403784438,-0.4,-0.15));
#7345=CARTESIAN_POINT('',(0.0866025403784439,-0.64,-0.15));
#7346=CARTESIAN_POINT('Origin',(-0.173205080756888,-0.4,-2.77555756156289E-17));
#7347=CARTESIAN_POINT('',(-0.173205080756888,-0.4,-2.12115047744981E-17));
#7348=CARTESIAN_POINT('',(-0.0866025403784438,-0.4,-0.15));
#7349=CARTESIAN_POINT('',(-0.173205080756888,-0.64,-2.77555756156289E-17));
#7350=CARTESIAN_POINT('',(-0.173205080756888,-0.4,-2.12115047744981E-17));
#7351=CARTESIAN_POINT('',(-0.0866025403784438,-0.64,-0.15));
#7352=CARTESIAN_POINT('Origin',(-0.0866025403784439,-0.4,0.15));
#7353=CARTESIAN_POINT('',(-0.0866025403784439,-0.4,0.15));
#7354=CARTESIAN_POINT('',(-0.173205080756888,-0.4,-2.12115047744981E-17));
#7355=CARTESIAN_POINT('',(-0.0866025403784439,-0.64,0.15));
#7356=CARTESIAN_POINT('',(-0.0866025403784439,-0.4,0.15));
#7357=CARTESIAN_POINT('',(-0.173205080756888,-0.64,-2.12115047744981E-17));
#7358=CARTESIAN_POINT('Origin',(0.0866025403784439,-0.4,0.15));
#7359=CARTESIAN_POINT('',(0.0866025403784439,-0.4,0.15));
#7360=CARTESIAN_POINT('',(-0.0866025403784439,-0.4,0.15));
#7361=CARTESIAN_POINT('',(0.0866025403784439,-0.64,0.15));
#7362=CARTESIAN_POINT('',(0.0866025403784439,-0.4,0.15));
#7363=CARTESIAN_POINT('',(-0.0866025403784439,-0.64,0.15));
#7364=CARTESIAN_POINT('Origin',(0.173205080756888,-0.4,0.));
#7365=CARTESIAN_POINT('',(0.0866025403784439,-0.4,0.15));
#7366=CARTESIAN_POINT('',(0.0866025403784439,-0.64,0.15));
#7367=CARTESIAN_POINT('Origin',(0.,-0.4,-2.77555756156289E-17));
#7368=CARTESIAN_POINT('Origin',(0.,-0.64,-2.77555756156289E-17));
#7369=CARTESIAN_POINT('Origin',(0.,-1.,0.));
#7370=CARTESIAN_POINT('',(-0.1954,-1.,2.39295984553393E-17));
#7371=CARTESIAN_POINT('Origin',(0.,-1.,0.));
#7372=CARTESIAN_POINT('Origin',(0.3,0.4,0.));
#7373=CARTESIAN_POINT('',(-0.3,0.4,-3.67394039744206E-17));
#7374=CARTESIAN_POINT('Origin',(0.,0.4,0.));
#7375=CARTESIAN_POINT('Origin',(0.,0.375,0.));
#7376=CARTESIAN_POINT('',(-0.35,0.35,-4.28626379701573E-17));
#7377=CARTESIAN_POINT('Origin',(0.,0.35,0.));
#7378=CARTESIAN_POINT('',(-0.325,0.375,-3.9801020972289E-17));
#7379=CARTESIAN_POINT('Origin',(0.,0.19,0.));
#7380=CARTESIAN_POINT('',(-0.35,0.03,-4.28626379701574E-17));
#7381=CARTESIAN_POINT('Origin',(0.,0.03,0.));
#7382=CARTESIAN_POINT('',(-0.35,0.19,-4.28626379701574E-17));
#7383=CARTESIAN_POINT('Origin',(0.,0.0149999999999999,0.));
#7384=CARTESIAN_POINT('',(-0.32,-3.29597460435593E-17,-3.91886975727153E-17));
#7385=CARTESIAN_POINT('Origin',(0.,0.,0.));
#7386=CARTESIAN_POINT('',(-0.335,0.0149999999999999,-4.10256677714363E-17));
#7387=CARTESIAN_POINT('Origin',(0.22,0.,0.));
#7388=CARTESIAN_POINT('',(-0.22,-6.93889390390723E-18,-2.69422295812418E-17));
#7389=CARTESIAN_POINT('Origin',(0.,0.,0.));
#7390=CARTESIAN_POINT('Origin',(0.,-0.02,0.));
#7391=CARTESIAN_POINT('',(-0.1954,-0.0492,2.39295984553393E-17));
#7392=CARTESIAN_POINT('Origin',(0.,-0.0492,0.));
#7393=CARTESIAN_POINT('',(-0.21,-0.02,-2.57175827820944E-17));
#7394=CARTESIAN_POINT('Origin',(0.,-0.8,0.));
#7395=CARTESIAN_POINT('',(-0.1954,-0.8,-2.39295984553393E-17));
#7574=UNCERTAINTY_MEASURE_WITH_UNIT(LENGTH_MEASURE(0.001),#7610,
'DISTANCE_ACCURACY_VALUE',
'Maximum model space distance between geometric entities at asserted c
onnectivities');
#7579=UNCERTAINTY_MEASURE_WITH_UNIT(LENGTH_MEASURE(0.001),#7610,
'DISTANCE_ACCURACY_VALUE',
'Maximum model space distance between geometric entities at asserted c
onnectivities');
#7604=(
GEOMETRIC_REPRESENTATION_CONTEXT(3)
GLOBAL_UNCERTAINTY_ASSIGNED_CONTEXT((#7574))
GLOBAL_UNIT_ASSIGNED_CONTEXT((#7610,#7612,#7613))
REPRESENTATION_CONTEXT('','3D')
);
#7609=(
GEOMETRIC_REPRESENTATION_CONTEXT(3)
GLOBAL_UNCERTAINTY_ASSIGNED_CONTEXT((#7579))
GLOBAL_UNIT_ASSIGNED_CONTEXT((#7610,#7612,#7613))
REPRESENTATION_CONTEXT('','3D')
);
#7610=(
LENGTH_UNIT()
NAMED_UNIT(*)
SI_UNIT(.CENTI.,.METRE.)
);
#7612=(
NAMED_UNIT(*)
PLANE_ANGLE_UNIT()
SI_UNIT($,.RADIAN.)
);
#7613=(
NAMED_UNIT(*)
SI_UNIT($,.STERADIAN.)
SOLID_ANGLE_UNIT()
);
#7638=SHAPE_DEFINITION_REPRESENTATION(#7695,#7744);
#7695=PRODUCT_DEFINITION_SHAPE('',$,#7774);
#7744=SHAPE_REPRESENTATION('',(#4662),#7604);
#7749=PRODUCT_DEFINITION_CONTEXT('part definition',#7838,'design');
#7774=PRODUCT_DEFINITION('M4x10 Cap Screw','M4x10 Cap Screw',#7803,#7749);
#7803=PRODUCT_DEFINITION_FORMATION('',$,#7864);
#7838=APPLICATION_CONTEXT(
'Core Data for Automotive Mechanical Design Process');
#7839=PRODUCT_CONTEXT('part definition',#7838,'mechanical');
#7864=PRODUCT('M4x10 Cap Screw','M4x10 Cap Screw','M4x10 Cap Screw',(#7839));
#7932=COLOUR_RGB('Black',0.12,0.14,0.17);
#7933=FILL_AREA_STYLE_COLOUR('',#7932);
#7934=FILL_AREA_STYLE('',(#7933));
#7935=SURFACE_STYLE_FILL_AREA(#7934);
#7936=SURFACE_SIDE_STYLE('',(#7935));
#7937=SURFACE_STYLE_USAGE(.BOTH.,#7936);
#7938=PRESENTATION_STYLE_ASSIGNMENT((#7937));
ENDSEC;
END-ISO-10303-21;
